ISO-10303-21;
HEADER;
/* Generated by software containing ST-Developer
 * from STEP Tools, Inc. (www.steptools.com) 
 */

FILE_DESCRIPTION(
/* description */ ('Independent30mm screw-fed quill/spindle unit with16mm straight tool s
ocket, radial set screw, native reusable open ball bearings, retained 
inner/outer race stacks, keyed quill guide and M12x1.75 fine feed. Ext
ernal moving drive and tool not included. Ideal cage orbital links; in
dividual ball spin, force and preload not simulated. No drilling capac
ity, runout, speed, torque, load, life or machine safety rating.'),
/* implementation_level */ '2;1');

FILE_NAME(
/* name */ 'Feed thrust washer.step',
/* time_stamp */ '2026-11-08T18:59:42-08:00',
/* author */ (''),
/* organization */ (''),
/* preprocessor_version */ 'ST-DEVELOPER v20.2',
/* originating_system */ 'Autodesk Translation Framework v15.17.0.0',
/* authorisation */ '');

FILE_SCHEMA (('AUTOMOTIVE_DESIGN { 1 0 10303 214 3 1 1 }'));
ENDSEC;

DATA;
#10=MECHANICAL_DESIGN_GEOMETRIC_PRESENTATION_REPRESENTATION('',(#1608),#63898);
#1572=SHAPE_REPRESENTATION_RELATIONSHIP('SRR','None',#64011,#1590);
#1590=ADVANCED_BREP_SHAPE_REPRESENTATION('',(#1626),#63896);
#1608=STYLED_ITEM('',(#64097),#1626);
#1626=MANIFOLD_SOLID_BREP('Body1',#15494);
#1711=FACE_BOUND('',#4370,.T.);
#1712=FACE_BOUND('',#4372,.T.);
#2343=CYLINDRICAL_SURFACE('',#16744,6.);
#2344=CYLINDRICAL_SURFACE('',#16747,12.);
#2649=CIRCLE('',#16745,6.);
#2650=CIRCLE('',#16746,6.);
#2651=CIRCLE('',#16748,12.);
#2652=CIRCLE('',#16749,12.);
#3446=FACE_OUTER_BOUND('',#4367,.T.);
#3447=FACE_OUTER_BOUND('',#4368,.T.);
#3448=FACE_OUTER_BOUND('',#4369,.T.);
#3449=FACE_OUTER_BOUND('',#4371,.T.);
#4367=EDGE_LOOP('',(#14234,#14235,#14236,#14237));
#4368=EDGE_LOOP('',(#14238,#14239,#14240,#14241));
#4369=EDGE_LOOP('',(#14242));
#4370=EDGE_LOOP('',(#14243));
#4371=EDGE_LOOP('',(#14244));
#4372=EDGE_LOOP('',(#14245));
#5132=LINE('',#61218,#5895);
#5133=LINE('',#61224,#5896);
#5895=VECTOR('',#19670,6.);
#5896=VECTOR('',#19677,12.);
#7419=VERTEX_POINT('',#61215);
#7420=VERTEX_POINT('',#61217);
#7421=VERTEX_POINT('',#61221);
#7422=VERTEX_POINT('',#61223);
#9706=EDGE_CURVE('',#7419,#7419,#2649,.T.);
#9707=EDGE_CURVE('',#7419,#7420,#5132,.T.);
#9708=EDGE_CURVE('',#7420,#7420,#2650,.T.);
#9709=EDGE_CURVE('',#7421,#7421,#2651,.T.);
#9710=EDGE_CURVE('',#7421,#7422,#5133,.T.);
#9711=EDGE_CURVE('',#7422,#7422,#2652,.T.);
#14234=ORIENTED_EDGE('',*,*,#9706,.F.);
#14235=ORIENTED_EDGE('',*,*,#9707,.T.);
#14236=ORIENTED_EDGE('',*,*,#9708,.T.);
#14237=ORIENTED_EDGE('',*,*,#9707,.F.);
#14238=ORIENTED_EDGE('',*,*,#9709,.F.);
#14239=ORIENTED_EDGE('',*,*,#9710,.T.);
#14240=ORIENTED_EDGE('',*,*,#9711,.T.);
#14241=ORIENTED_EDGE('',*,*,#9710,.F.);
#14242=ORIENTED_EDGE('',*,*,#9709,.T.);
#14243=ORIENTED_EDGE('',*,*,#9706,.T.);
#14244=ORIENTED_EDGE('',*,*,#9711,.F.);
#14245=ORIENTED_EDGE('',*,*,#9708,.F.);
#14628=PLANE('',#16750);
#14629=PLANE('',#16751);
#15426=ADVANCED_FACE('',(#3446),#2343,.F.);
#15427=ADVANCED_FACE('',(#3447),#2344,.T.);
#15428=ADVANCED_FACE('',(#3448,#1711),#14628,.T.);
#15429=ADVANCED_FACE('',(#3449,#1712),#14629,.F.);
#15494=CLOSED_SHELL('',(#15426,#15427,#15428,#15429));
#16743=AXIS2_PLACEMENT_3D('',#61213,#19664,#19665);
#16744=AXIS2_PLACEMENT_3D('',#61214,#19666,#19667);
#16745=AXIS2_PLACEMENT_3D('',#61216,#19668,#19669);
#16746=AXIS2_PLACEMENT_3D('',#61219,#19671,#19672);
#16747=AXIS2_PLACEMENT_3D('',#61220,#19673,#19674);
#16748=AXIS2_PLACEMENT_3D('',#61222,#19675,#19676);
#16749=AXIS2_PLACEMENT_3D('',#61225,#19678,#19679);
#16750=AXIS2_PLACEMENT_3D('',#61226,#19680,#19681);
#16751=AXIS2_PLACEMENT_3D('',#61227,#19682,#19683);
#19664=DIRECTION('axis',(0.,0.,1.));
#19665=DIRECTION('refdir',(1.,0.,0.));
#19666=DIRECTION('center_axis',(0.,0.,1.));
#19667=DIRECTION('ref_axis',(1.,0.,0.));
#19668=DIRECTION('center_axis',(0.,0.,-1.));
#19669=DIRECTION('ref_axis',(1.,0.,0.));
#19670=DIRECTION('',(0.,0.,-1.));
#19671=DIRECTION('center_axis',(0.,0.,-1.));
#19672=DIRECTION('ref_axis',(1.,0.,0.));
#19673=DIRECTION('center_axis',(0.,0.,1.));
#19674=DIRECTION('ref_axis',(1.,0.,0.));
#19675=DIRECTION('center_axis',(0.,0.,1.));
#19676=DIRECTION('ref_axis',(1.,0.,0.));
#19677=DIRECTION('',(0.,0.,-1.));
#19678=DIRECTION('center_axis',(0.,0.,1.));
#19679=DIRECTION('ref_axis',(1.,0.,0.));
#19680=DIRECTION('center_axis',(0.,0.,1.));
#19681=DIRECTION('ref_axis',(1.,0.,0.));
#19682=DIRECTION('center_axis',(0.,0.,1.));
#19683=DIRECTION('ref_axis',(1.,0.,0.));
#61213=CARTESIAN_POINT('',(0.,0.,0.));
#61214=CARTESIAN_POINT('Origin',(0.,0.,0.));
#61215=CARTESIAN_POINT('',(-6.,-7.34788079488412E-16,2.));
#61216=CARTESIAN_POINT('Origin',(0.,0.,2.));
#61217=CARTESIAN_POINT('',(-6.,-7.34788079488412E-16,0.));
#61218=CARTESIAN_POINT('',(-6.,-7.34788079488412E-16,0.));
#61219=CARTESIAN_POINT('Origin',(0.,0.,0.));
#61220=CARTESIAN_POINT('Origin',(0.,0.,0.));
#61221=CARTESIAN_POINT('',(-12.,-1.46957615897682E-15,2.));
#61222=CARTESIAN_POINT('Origin',(0.,0.,2.));
#61223=CARTESIAN_POINT('',(-12.,-1.46957615897682E-15,0.));
#61224=CARTESIAN_POINT('',(-12.,-1.46957615897682E-15,0.));
#61225=CARTESIAN_POINT('Origin',(0.,0.,0.));
#61226=CARTESIAN_POINT('Origin',(0.,0.,2.));
#61227=CARTESIAN_POINT('Origin',(0.,0.,0.));
#63876=UNCERTAINTY_MEASURE_WITH_UNIT(LENGTH_MEASURE(0.01),#63899,
'DISTANCE_ACCURACY_VALUE',
'Maximum model space distance between geometric entities at asserted c
onnectivities');
#63878=UNCERTAINTY_MEASURE_WITH_UNIT(LENGTH_MEASURE(0.01),#63899,
'DISTANCE_ACCURACY_VALUE',
'Maximum model space distance between geometric entities at asserted c
onnectivities');
#63896=(
GEOMETRIC_REPRESENTATION_CONTEXT(3)
GLOBAL_UNCERTAINTY_ASSIGNED_CONTEXT((#63876))
GLOBAL_UNIT_ASSIGNED_CONTEXT((#63899,#63901,#63902))
REPRESENTATION_CONTEXT('','3D')
);
#63898=(
GEOMETRIC_REPRESENTATION_CONTEXT(3)
GLOBAL_UNCERTAINTY_ASSIGNED_CONTEXT((#63878))
GLOBAL_UNIT_ASSIGNED_CONTEXT((#63899,#63901,#63902))
REPRESENTATION_CONTEXT('','3D')
);
#63899=(
LENGTH_UNIT()
NAMED_UNIT(*)
SI_UNIT(.MILLI.,.METRE.)
);
#63901=(
NAMED_UNIT(*)
PLANE_ANGLE_UNIT()
SI_UNIT($,.RADIAN.)
);
#63902=(
NAMED_UNIT(*)
SI_UNIT($,.STERADIAN.)
SOLID_ANGLE_UNIT()
);
#63920=SHAPE_DEFINITION_REPRESENTATION(#63939,#64011);
#63939=PRODUCT_DEFINITION_SHAPE('',$,#64031);
#64011=SHAPE_REPRESENTATION('',(#16743),#63896);
#64013=PRODUCT_DEFINITION_CONTEXT('part definition',#64072,'design');
#64031=PRODUCT_DEFINITION('Feed thrust washer','Feed thrust washer',#64050,
#64013);
#64050=PRODUCT_DEFINITION_FORMATION('',$,#64091);
#64072=APPLICATION_CONTEXT(
'Core Data for Automotive Mechanical Design Process');
#64073=PRODUCT_CONTEXT('part definition',#64072,'mechanical');
#64091=PRODUCT('Feed thrust washer','Feed thrust washer',$,(#64073));
#64097=PRESENTATION_STYLE_ASSIGNMENT((#64110));
#64110=SURFACE_STYLE_USAGE(.BOTH.,#64123);
#64123=SURFACE_SIDE_STYLE('',(#64136));
#64136=SURFACE_STYLE_FILL_AREA(#64149);
#64149=FILL_AREA_STYLE('Light gray',(#64162));
#64162=FILL_AREA_STYLE_COLOUR('Light gray',#64175);
#64175=COLOUR_RGB('Light gray',0.725490196078431,0.752941176470588,0.792156862745098);
ENDSEC;
END-ISO-10303-21;
